ISO-10303-21;
HEADER;
/* Generated by software containing ST-Developer
 * from STEP Tools, Inc. (www.steptools.com) 
 */

FILE_DESCRIPTION(
/* description */ ('Grid plate located blocks and clamp'),
/* implementation_level */ '2;1');

FILE_NAME(
/* name */ 'Captive-nut hand knob.step',
/* time_stamp */ '2026-10-29T15:43:47-07:00',
/* author */ (''),
/* organization */ (''),
/* preprocessor_version */ 'ST-DEVELOPER v20.2',
/* originating_system */ 'Autodesk Translation Framework v15.17.0.0',
/* authorisation */ '');

FILE_SCHEMA (('AUTOMOTIVE_DESIGN { 1 0 10303 214 3 1 1 }'));
ENDSEC;

DATA;
#10=MECHANICAL_DESIGN_GEOMETRIC_PRESENTATION_REPRESENTATION('',(#179),#5702);
#153=SHAPE_REPRESENTATION_RELATIONSHIP('SRR','None',#5771,#165);
#165=ADVANCED_BREP_SHAPE_REPRESENTATION('',(#191),#5701);
#179=STYLED_ITEM('',(#5904),#191);
#191=MANIFOLD_SOLID_BREP('Body1',#3276);
#265=FACE_BOUND('',#881,.T.);
#266=FACE_BOUND('',#895,.T.);
#267=FACE_BOUND('',#898,.T.);
#371=CIRCLE('',#3690,0.4);
#372=CIRCLE('',#3691,0.4);
#373=CIRCLE('',#3693,0.4);
#374=CIRCLE('',#3694,0.4);
#375=CIRCLE('',#3696,0.4);
#376=CIRCLE('',#3697,0.4);
#377=CIRCLE('',#3699,0.4);
#378=CIRCLE('',#3700,0.4);
#379=CIRCLE('',#3702,0.4);
#380=CIRCLE('',#3703,0.4);
#381=CIRCLE('',#3705,0.4);
#382=CIRCLE('',#3706,0.4);
#383=CIRCLE('',#3708,1.8);
#384=CIRCLE('',#3709,1.8);
#385=CIRCLE('',#3710,1.8);
#386=CIRCLE('',#3711,1.8);
#387=CIRCLE('',#3712,1.8);
#388=CIRCLE('',#3713,1.8);
#389=CIRCLE('',#3714,0.425);
#390=CIRCLE('',#3716,1.8);
#391=CIRCLE('',#3718,1.8);
#392=CIRCLE('',#3720,1.8);
#393=CIRCLE('',#3722,1.8);
#394=CIRCLE('',#3724,1.8);
#395=CIRCLE('',#3726,1.8);
#396=CIRCLE('',#3734,0.425);
#444=CYLINDRICAL_SURFACE('',#3689,0.4);
#445=CYLINDRICAL_SURFACE('',#3692,0.4);
#446=CYLINDRICAL_SURFACE('',#3695,0.4);
#447=CYLINDRICAL_SURFACE('',#3698,0.4);
#448=CYLINDRICAL_SURFACE('',#3701,0.4);
#449=CYLINDRICAL_SURFACE('',#3704,0.4);
#450=CYLINDRICAL_SURFACE('',#3715,1.8);
#451=CYLINDRICAL_SURFACE('',#3717,1.8);
#452=CYLINDRICAL_SURFACE('',#3719,1.8);
#453=CYLINDRICAL_SURFACE('',#3721,1.8);
#454=CYLINDRICAL_SURFACE('',#3723,1.8);
#455=CYLINDRICAL_SURFACE('',#3725,1.8);
#456=CYLINDRICAL_SURFACE('',#3735,0.425);
#618=FACE_OUTER_BOUND('',#874,.T.);
#619=FACE_OUTER_BOUND('',#875,.T.);
#620=FACE_OUTER_BOUND('',#876,.T.);
#621=FACE_OUTER_BOUND('',#877,.T.);
#622=FACE_OUTER_BOUND('',#878,.T.);
#623=FACE_OUTER_BOUND('',#879,.T.);
#624=FACE_OUTER_BOUND('',#880,.T.);
#625=FACE_OUTER_BOUND('',#882,.T.);
#626=FACE_OUTER_BOUND('',#883,.T.);
#627=FACE_OUTER_BOUND('',#884,.T.);
#628=FACE_OUTER_BOUND('',#885,.T.);
#629=FACE_OUTER_BOUND('',#886,.T.);
#630=FACE_OUTER_BOUND('',#887,.T.);
#631=FACE_OUTER_BOUND('',#888,.T.);
#632=FACE_OUTER_BOUND('',#889,.T.);
#633=FACE_OUTER_BOUND('',#890,.T.);
#634=FACE_OUTER_BOUND('',#891,.T.);
#635=FACE_OUTER_BOUND('',#892,.T.);
#636=FACE_OUTER_BOUND('',#893,.T.);
#637=FACE_OUTER_BOUND('',#894,.T.);
#638=FACE_OUTER_BOUND('',#896,.T.);
#639=FACE_OUTER_BOUND('',#897,.T.);
#874=EDGE_LOOP('',(#2850,#2851,#2852,#2853));
#875=EDGE_LOOP('',(#2854,#2855,#2856,#2857));
#876=EDGE_LOOP('',(#2858,#2859,#2860,#2861));
#877=EDGE_LOOP('',(#2862,#2863,#2864,#2865));
#878=EDGE_LOOP('',(#2866,#2867,#2868,#2869));
#879=EDGE_LOOP('',(#2870,#2871,#2872,#2873));
#880=EDGE_LOOP('',(#2874,#2875,#2876,#2877,#2878,#2879,#2880,#2881,#2882,
#2883,#2884,#2885));
#881=EDGE_LOOP('',(#2886));
#882=EDGE_LOOP('',(#2887,#2888,#2889,#2890));
#883=EDGE_LOOP('',(#2891,#2892,#2893,#2894));
#884=EDGE_LOOP('',(#2895,#2896,#2897,#2898));
#885=EDGE_LOOP('',(#2899,#2900,#2901,#2902));
#886=EDGE_LOOP('',(#2903,#2904,#2905,#2906));
#887=EDGE_LOOP('',(#2907,#2908,#2909,#2910));
#888=EDGE_LOOP('',(#2911,#2912,#2913,#2914));
#889=EDGE_LOOP('',(#2915,#2916,#2917,#2918));
#890=EDGE_LOOP('',(#2919,#2920,#2921,#2922));
#891=EDGE_LOOP('',(#2923,#2924,#2925,#2926));
#892=EDGE_LOOP('',(#2927,#2928,#2929,#2930));
#893=EDGE_LOOP('',(#2931,#2932,#2933,#2934));
#894=EDGE_LOOP('',(#2935,#2936,#2937,#2938,#2939,#2940));
#895=EDGE_LOOP('',(#2941));
#896=EDGE_LOOP('',(#2942,#2943,#2944,#2945));
#897=EDGE_LOOP('',(#2946,#2947,#2948,#2949,#2950,#2951,#2952,#2953,#2954,
#2955,#2956,#2957));
#898=EDGE_LOOP('',(#2958,#2959,#2960,#2961,#2962,#2963));
#1141=LINE('',#5535,#1414);
#1142=LINE('',#5539,#1415);
#1143=LINE('',#5544,#1416);
#1144=LINE('',#5548,#1417);
#1145=LINE('',#5553,#1418);
#1146=LINE('',#5557,#1419);
#1147=LINE('',#5562,#1420);
#1148=LINE('',#5566,#1421);
#1149=LINE('',#5571,#1422);
#1150=LINE('',#5575,#1423);
#1151=LINE('',#5580,#1424);
#1152=LINE('',#5584,#1425);
#1153=LINE('',#5610,#1426);
#1154=LINE('',#5612,#1427);
#1155=LINE('',#5614,#1428);
#1156=LINE('',#5615,#1429);
#1157=LINE('',#5618,#1430);
#1158=LINE('',#5620,#1431);
#1159=LINE('',#5621,#1432);
#1160=LINE('',#5624,#1433);
#1161=LINE('',#5626,#1434);
#1162=LINE('',#5627,#1435);
#1163=LINE('',#5630,#1436);
#1164=LINE('',#5632,#1437);
#1165=LINE('',#5633,#1438);
#1166=LINE('',#5636,#1439);
#1167=LINE('',#5638,#1440);
#1168=LINE('',#5639,#1441);
#1169=LINE('',#5641,#1442);
#1170=LINE('',#5642,#1443);
#1171=LINE('',#5647,#1444);
#1414=VECTOR('',#4565,1.);
#1415=VECTOR('',#4568,1.);
#1416=VECTOR('',#4573,1.);
#1417=VECTOR('',#4576,1.);
#1418=VECTOR('',#4581,1.);
#1419=VECTOR('',#4584,1.);
#1420=VECTOR('',#4589,1.);
#1421=VECTOR('',#4592,1.);
#1422=VECTOR('',#4597,1.);
#1423=VECTOR('',#4600,1.);
#1424=VECTOR('',#4605,1.);
#1425=VECTOR('',#4608,1.);
#1426=VECTOR('',#4653,1.);
#1427=VECTOR('',#4654,1.);
#1428=VECTOR('',#4655,1.);
#1429=VECTOR('',#4656,1.);
#1430=VECTOR('',#4659,1.);
#1431=VECTOR('',#4660,1.);
#1432=VECTOR('',#4661,1.);
#1433=VECTOR('',#4664,1.);
#1434=VECTOR('',#4665,1.);
#1435=VECTOR('',#4666,1.);
#1436=VECTOR('',#4669,1.);
#1437=VECTOR('',#4670,1.);
#1438=VECTOR('',#4671,1.);
#1439=VECTOR('',#4674,1.);
#1440=VECTOR('',#4675,1.);
#1441=VECTOR('',#4676,1.);
#1442=VECTOR('',#4679,1.);
#1443=VECTOR('',#4680,1.);
#1444=VECTOR('',#4687,0.425);
#1678=VERTEX_POINT('',#5533);
#1679=VERTEX_POINT('',#5534);
#1680=VERTEX_POINT('',#5536);
#1681=VERTEX_POINT('',#5538);
#1682=VERTEX_POINT('',#5542);
#1683=VERTEX_POINT('',#5543);
#1684=VERTEX_POINT('',#5545);
#1685=VERTEX_POINT('',#5547);
#1686=VERTEX_POINT('',#5551);
#1687=VERTEX_POINT('',#5552);
#1688=VERTEX_POINT('',#5554);
#1689=VERTEX_POINT('',#5556);
#1690=VERTEX_POINT('',#5560);
#1691=VERTEX_POINT('',#5561);
#1692=VERTEX_POINT('',#5563);
#1693=VERTEX_POINT('',#5565);
#1694=VERTEX_POINT('',#5569);
#1695=VERTEX_POINT('',#5570);
#1696=VERTEX_POINT('',#5572);
#1697=VERTEX_POINT('',#5574);
#1698=VERTEX_POINT('',#5578);
#1699=VERTEX_POINT('',#5579);
#1700=VERTEX_POINT('',#5581);
#1701=VERTEX_POINT('',#5583);
#1702=VERTEX_POINT('',#5593);
#1703=VERTEX_POINT('',#5608);
#1704=VERTEX_POINT('',#5609);
#1705=VERTEX_POINT('',#5611);
#1706=VERTEX_POINT('',#5613);
#1707=VERTEX_POINT('',#5617);
#1708=VERTEX_POINT('',#5619);
#1709=VERTEX_POINT('',#5623);
#1710=VERTEX_POINT('',#5625);
#1711=VERTEX_POINT('',#5629);
#1712=VERTEX_POINT('',#5631);
#1713=VERTEX_POINT('',#5635);
#1714=VERTEX_POINT('',#5637);
#1715=VERTEX_POINT('',#5644);
#2075=EDGE_CURVE('',#1678,#1679,#1141,.T.);
#2076=EDGE_CURVE('',#1680,#1678,#371,.T.);
#2077=EDGE_CURVE('',#1681,#1680,#1142,.T.);
#2078=EDGE_CURVE('',#1679,#1681,#372,.T.);
#2079=EDGE_CURVE('',#1682,#1683,#1143,.T.);
#2080=EDGE_CURVE('',#1684,#1682,#373,.T.);
#2081=EDGE_CURVE('',#1685,#1684,#1144,.T.);
#2082=EDGE_CURVE('',#1683,#1685,#374,.T.);
#2083=EDGE_CURVE('',#1686,#1687,#1145,.T.);
#2084=EDGE_CURVE('',#1688,#1686,#375,.T.);
#2085=EDGE_CURVE('',#1689,#1688,#1146,.T.);
#2086=EDGE_CURVE('',#1687,#1689,#376,.T.);
#2087=EDGE_CURVE('',#1690,#1691,#1147,.T.);
#2088=EDGE_CURVE('',#1692,#1690,#377,.T.);
#2089=EDGE_CURVE('',#1693,#1692,#1148,.T.);
#2090=EDGE_CURVE('',#1691,#1693,#378,.T.);
#2091=EDGE_CURVE('',#1694,#1695,#1149,.T.);
#2092=EDGE_CURVE('',#1696,#1694,#379,.T.);
#2093=EDGE_CURVE('',#1697,#1696,#1150,.T.);
#2094=EDGE_CURVE('',#1695,#1697,#380,.T.);
#2095=EDGE_CURVE('',#1698,#1699,#1151,.T.);
#2096=EDGE_CURVE('',#1700,#1698,#381,.T.);
#2097=EDGE_CURVE('',#1701,#1700,#1152,.T.);
#2098=EDGE_CURVE('',#1699,#1701,#382,.T.);
#2099=EDGE_CURVE('',#1678,#1700,#383,.T.);
#2100=EDGE_CURVE('',#1698,#1683,#384,.T.);
#2101=EDGE_CURVE('',#1685,#1688,#385,.T.);
#2102=EDGE_CURVE('',#1686,#1692,#386,.T.);
#2103=EDGE_CURVE('',#1690,#1696,#387,.T.);
#2104=EDGE_CURVE('',#1694,#1680,#388,.T.);
#2105=EDGE_CURVE('',#1702,#1702,#389,.T.);
#2106=EDGE_CURVE('',#1691,#1697,#390,.T.);
#2107=EDGE_CURVE('',#1687,#1693,#391,.T.);
#2108=EDGE_CURVE('',#1699,#1682,#392,.T.);
#2109=EDGE_CURVE('',#1684,#1689,#393,.T.);
#2110=EDGE_CURVE('',#1679,#1701,#394,.T.);
#2111=EDGE_CURVE('',#1695,#1681,#395,.T.);
#2112=EDGE_CURVE('',#1703,#1704,#1153,.T.);
#2113=EDGE_CURVE('',#1703,#1705,#1154,.T.);
#2114=EDGE_CURVE('',#1705,#1706,#1155,.T.);
#2115=EDGE_CURVE('',#1704,#1706,#1156,.T.);
#2116=EDGE_CURVE('',#1704,#1707,#1157,.T.);
#2117=EDGE_CURVE('',#1706,#1708,#1158,.T.);
#2118=EDGE_CURVE('',#1707,#1708,#1159,.T.);
#2119=EDGE_CURVE('',#1707,#1709,#1160,.T.);
#2120=EDGE_CURVE('',#1708,#1710,#1161,.T.);
#2121=EDGE_CURVE('',#1709,#1710,#1162,.T.);
#2122=EDGE_CURVE('',#1709,#1711,#1163,.T.);
#2123=EDGE_CURVE('',#1710,#1712,#1164,.T.);
#2124=EDGE_CURVE('',#1711,#1712,#1165,.T.);
#2125=EDGE_CURVE('',#1713,#1703,#1166,.T.);
#2126=EDGE_CURVE('',#1713,#1714,#1167,.T.);
#2127=EDGE_CURVE('',#1714,#1705,#1168,.T.);
#2128=EDGE_CURVE('',#1711,#1713,#1169,.T.);
#2129=EDGE_CURVE('',#1712,#1714,#1170,.T.);
#2130=EDGE_CURVE('',#1715,#1715,#396,.T.);
#2131=EDGE_CURVE('',#1702,#1715,#1171,.T.);
#2850=ORIENTED_EDGE('',*,*,#2075,.F.);
#2851=ORIENTED_EDGE('',*,*,#2076,.F.);
#2852=ORIENTED_EDGE('',*,*,#2077,.F.);
#2853=ORIENTED_EDGE('',*,*,#2078,.F.);
#2854=ORIENTED_EDGE('',*,*,#2079,.F.);
#2855=ORIENTED_EDGE('',*,*,#2080,.F.);
#2856=ORIENTED_EDGE('',*,*,#2081,.F.);
#2857=ORIENTED_EDGE('',*,*,#2082,.F.);
#2858=ORIENTED_EDGE('',*,*,#2083,.F.);
#2859=ORIENTED_EDGE('',*,*,#2084,.F.);
#2860=ORIENTED_EDGE('',*,*,#2085,.F.);
#2861=ORIENTED_EDGE('',*,*,#2086,.F.);
#2862=ORIENTED_EDGE('',*,*,#2087,.F.);
#2863=ORIENTED_EDGE('',*,*,#2088,.F.);
#2864=ORIENTED_EDGE('',*,*,#2089,.F.);
#2865=ORIENTED_EDGE('',*,*,#2090,.F.);
#2866=ORIENTED_EDGE('',*,*,#2091,.F.);
#2867=ORIENTED_EDGE('',*,*,#2092,.F.);
#2868=ORIENTED_EDGE('',*,*,#2093,.F.);
#2869=ORIENTED_EDGE('',*,*,#2094,.F.);
#2870=ORIENTED_EDGE('',*,*,#2095,.F.);
#2871=ORIENTED_EDGE('',*,*,#2096,.F.);
#2872=ORIENTED_EDGE('',*,*,#2097,.F.);
#2873=ORIENTED_EDGE('',*,*,#2098,.F.);
#2874=ORIENTED_EDGE('',*,*,#2076,.T.);
#2875=ORIENTED_EDGE('',*,*,#2099,.T.);
#2876=ORIENTED_EDGE('',*,*,#2096,.T.);
#2877=ORIENTED_EDGE('',*,*,#2100,.T.);
#2878=ORIENTED_EDGE('',*,*,#2082,.T.);
#2879=ORIENTED_EDGE('',*,*,#2101,.T.);
#2880=ORIENTED_EDGE('',*,*,#2084,.T.);
#2881=ORIENTED_EDGE('',*,*,#2102,.T.);
#2882=ORIENTED_EDGE('',*,*,#2088,.T.);
#2883=ORIENTED_EDGE('',*,*,#2103,.T.);
#2884=ORIENTED_EDGE('',*,*,#2092,.T.);
#2885=ORIENTED_EDGE('',*,*,#2104,.T.);
#2886=ORIENTED_EDGE('',*,*,#2105,.T.);
#2887=ORIENTED_EDGE('',*,*,#2087,.T.);
#2888=ORIENTED_EDGE('',*,*,#2106,.T.);
#2889=ORIENTED_EDGE('',*,*,#2093,.T.);
#2890=ORIENTED_EDGE('',*,*,#2103,.F.);
#2891=ORIENTED_EDGE('',*,*,#2083,.T.);
#2892=ORIENTED_EDGE('',*,*,#2107,.T.);
#2893=ORIENTED_EDGE('',*,*,#2089,.T.);
#2894=ORIENTED_EDGE('',*,*,#2102,.F.);
#2895=ORIENTED_EDGE('',*,*,#2079,.T.);
#2896=ORIENTED_EDGE('',*,*,#2100,.F.);
#2897=ORIENTED_EDGE('',*,*,#2095,.T.);
#2898=ORIENTED_EDGE('',*,*,#2108,.T.);
#2899=ORIENTED_EDGE('',*,*,#2081,.T.);
#2900=ORIENTED_EDGE('',*,*,#2109,.T.);
#2901=ORIENTED_EDGE('',*,*,#2085,.T.);
#2902=ORIENTED_EDGE('',*,*,#2101,.F.);
#2903=ORIENTED_EDGE('',*,*,#2075,.T.);
#2904=ORIENTED_EDGE('',*,*,#2110,.T.);
#2905=ORIENTED_EDGE('',*,*,#2097,.T.);
#2906=ORIENTED_EDGE('',*,*,#2099,.F.);
#2907=ORIENTED_EDGE('',*,*,#2077,.T.);
#2908=ORIENTED_EDGE('',*,*,#2104,.F.);
#2909=ORIENTED_EDGE('',*,*,#2091,.T.);
#2910=ORIENTED_EDGE('',*,*,#2111,.T.);
#2911=ORIENTED_EDGE('',*,*,#2112,.F.);
#2912=ORIENTED_EDGE('',*,*,#2113,.T.);
#2913=ORIENTED_EDGE('',*,*,#2114,.T.);
#2914=ORIENTED_EDGE('',*,*,#2115,.F.);
#2915=ORIENTED_EDGE('',*,*,#2116,.F.);
#2916=ORIENTED_EDGE('',*,*,#2115,.T.);
#2917=ORIENTED_EDGE('',*,*,#2117,.T.);
#2918=ORIENTED_EDGE('',*,*,#2118,.F.);
#2919=ORIENTED_EDGE('',*,*,#2119,.F.);
#2920=ORIENTED_EDGE('',*,*,#2118,.T.);
#2921=ORIENTED_EDGE('',*,*,#2120,.T.);
#2922=ORIENTED_EDGE('',*,*,#2121,.F.);
#2923=ORIENTED_EDGE('',*,*,#2122,.F.);
#2924=ORIENTED_EDGE('',*,*,#2121,.T.);
#2925=ORIENTED_EDGE('',*,*,#2123,.T.);
#2926=ORIENTED_EDGE('',*,*,#2124,.F.);
#2927=ORIENTED_EDGE('',*,*,#2125,.F.);
#2928=ORIENTED_EDGE('',*,*,#2126,.T.);
#2929=ORIENTED_EDGE('',*,*,#2127,.T.);
#2930=ORIENTED_EDGE('',*,*,#2113,.F.);
#2931=ORIENTED_EDGE('',*,*,#2128,.F.);
#2932=ORIENTED_EDGE('',*,*,#2124,.T.);
#2933=ORIENTED_EDGE('',*,*,#2129,.T.);
#2934=ORIENTED_EDGE('',*,*,#2126,.F.);
#2935=ORIENTED_EDGE('',*,*,#2129,.F.);
#2936=ORIENTED_EDGE('',*,*,#2123,.F.);
#2937=ORIENTED_EDGE('',*,*,#2120,.F.);
#2938=ORIENTED_EDGE('',*,*,#2117,.F.);
#2939=ORIENTED_EDGE('',*,*,#2114,.F.);
#2940=ORIENTED_EDGE('',*,*,#2127,.F.);
#2941=ORIENTED_EDGE('',*,*,#2130,.F.);
#2942=ORIENTED_EDGE('',*,*,#2105,.F.);
#2943=ORIENTED_EDGE('',*,*,#2131,.T.);
#2944=ORIENTED_EDGE('',*,*,#2130,.T.);
#2945=ORIENTED_EDGE('',*,*,#2131,.F.);
#2946=ORIENTED_EDGE('',*,*,#2078,.T.);
#2947=ORIENTED_EDGE('',*,*,#2111,.F.);
#2948=ORIENTED_EDGE('',*,*,#2094,.T.);
#2949=ORIENTED_EDGE('',*,*,#2106,.F.);
#2950=ORIENTED_EDGE('',*,*,#2090,.T.);
#2951=ORIENTED_EDGE('',*,*,#2107,.F.);
#2952=ORIENTED_EDGE('',*,*,#2086,.T.);
#2953=ORIENTED_EDGE('',*,*,#2109,.F.);
#2954=ORIENTED_EDGE('',*,*,#2080,.T.);
#2955=ORIENTED_EDGE('',*,*,#2108,.F.);
#2956=ORIENTED_EDGE('',*,*,#2098,.T.);
#2957=ORIENTED_EDGE('',*,*,#2110,.F.);
#2958=ORIENTED_EDGE('',*,*,#2122,.T.);
#2959=ORIENTED_EDGE('',*,*,#2128,.T.);
#2960=ORIENTED_EDGE('',*,*,#2125,.T.);
#2961=ORIENTED_EDGE('',*,*,#2112,.T.);
#2962=ORIENTED_EDGE('',*,*,#2116,.T.);
#2963=ORIENTED_EDGE('',*,*,#2119,.T.);
#3069=PLANE('',#3707);
#3070=PLANE('',#3727);
#3071=PLANE('',#3728);
#3072=PLANE('',#3729);
#3073=PLANE('',#3730);
#3074=PLANE('',#3731);
#3075=PLANE('',#3732);
#3076=PLANE('',#3733);
#3077=PLANE('',#3736);
#3239=ADVANCED_FACE('',(#618),#444,.F.);
#3240=ADVANCED_FACE('',(#619),#445,.F.);
#3241=ADVANCED_FACE('',(#620),#446,.F.);
#3242=ADVANCED_FACE('',(#621),#447,.F.);
#3243=ADVANCED_FACE('',(#622),#448,.F.);
#3244=ADVANCED_FACE('',(#623),#449,.F.);
#3245=ADVANCED_FACE('',(#624,#265),#3069,.T.);
#3246=ADVANCED_FACE('',(#625),#450,.T.);
#3247=ADVANCED_FACE('',(#626),#451,.T.);
#3248=ADVANCED_FACE('',(#627),#452,.T.);
#3249=ADVANCED_FACE('',(#628),#453,.T.);
#3250=ADVANCED_FACE('',(#629),#454,.T.);
#3251=ADVANCED_FACE('',(#630),#455,.T.);
#3252=ADVANCED_FACE('',(#631),#3070,.F.);
#3253=ADVANCED_FACE('',(#632),#3071,.F.);
#3254=ADVANCED_FACE('',(#633),#3072,.F.);
#3255=ADVANCED_FACE('',(#634),#3073,.F.);
#3256=ADVANCED_FACE('',(#635),#3074,.F.);
#3257=ADVANCED_FACE('',(#636),#3075,.F.);
#3258=ADVANCED_FACE('',(#637,#266),#3076,.F.);
#3259=ADVANCED_FACE('',(#638),#456,.F.);
#3260=ADVANCED_FACE('',(#639,#267),#3077,.F.);
#3276=CLOSED_SHELL('',(#3239,#3240,#3241,#3242,#3243,#3244,#3245,#3246,
#3247,#3248,#3249,#3250,#3251,#3252,#3253,#3254,#3255,#3256,#3257,#3258,
#3259,#3260));
#3688=AXIS2_PLACEMENT_3D('',#5531,#4561,#4562);
#3689=AXIS2_PLACEMENT_3D('',#5532,#4563,#4564);
#3690=AXIS2_PLACEMENT_3D('',#5537,#4566,#4567);
#3691=AXIS2_PLACEMENT_3D('',#5540,#4569,#4570);
#3692=AXIS2_PLACEMENT_3D('',#5541,#4571,#4572);
#3693=AXIS2_PLACEMENT_3D('',#5546,#4574,#4575);
#3694=AXIS2_PLACEMENT_3D('',#5549,#4577,#4578);
#3695=AXIS2_PLACEMENT_3D('',#5550,#4579,#4580);
#3696=AXIS2_PLACEMENT_3D('',#5555,#4582,#4583);
#3697=AXIS2_PLACEMENT_3D('',#5558,#4585,#4586);
#3698=AXIS2_PLACEMENT_3D('',#5559,#4587,#4588);
#3699=AXIS2_PLACEMENT_3D('',#5564,#4590,#4591);
#3700=AXIS2_PLACEMENT_3D('',#5567,#4593,#4594);
#3701=AXIS2_PLACEMENT_3D('',#5568,#4595,#4596);
#3702=AXIS2_PLACEMENT_3D('',#5573,#4598,#4599);
#3703=AXIS2_PLACEMENT_3D('',#5576,#4601,#4602);
#3704=AXIS2_PLACEMENT_3D('',#5577,#4603,#4604);
#3705=AXIS2_PLACEMENT_3D('',#5582,#4606,#4607);
#3706=AXIS2_PLACEMENT_3D('',#5585,#4609,#4610);
#3707=AXIS2_PLACEMENT_3D('',#5586,#4611,#4612);
#3708=AXIS2_PLACEMENT_3D('',#5587,#4613,#4614);
#3709=AXIS2_PLACEMENT_3D('',#5588,#4615,#4616);
#3710=AXIS2_PLACEMENT_3D('',#5589,#4617,#4618);
#3711=AXIS2_PLACEMENT_3D('',#5590,#4619,#4620);
#3712=AXIS2_PLACEMENT_3D('',#5591,#4621,#4622);
#3713=AXIS2_PLACEMENT_3D('',#5592,#4623,#4624);
#3714=AXIS2_PLACEMENT_3D('',#5594,#4625,#4626);
#3715=AXIS2_PLACEMENT_3D('',#5595,#4627,#4628);
#3716=AXIS2_PLACEMENT_3D('',#5596,#4629,#4630);
#3717=AXIS2_PLACEMENT_3D('',#5597,#4631,#4632);
#3718=AXIS2_PLACEMENT_3D('',#5598,#4633,#4634);
#3719=AXIS2_PLACEMENT_3D('',#5599,#4635,#4636);
#3720=AXIS2_PLACEMENT_3D('',#5600,#4637,#4638);
#3721=AXIS2_PLACEMENT_3D('',#5601,#4639,#4640);
#3722=AXIS2_PLACEMENT_3D('',#5602,#4641,#4642);
#3723=AXIS2_PLACEMENT_3D('',#5603,#4643,#4644);
#3724=AXIS2_PLACEMENT_3D('',#5604,#4645,#4646);
#3725=AXIS2_PLACEMENT_3D('',#5605,#4647,#4648);
#3726=AXIS2_PLACEMENT_3D('',#5606,#4649,#4650);
#3727=AXIS2_PLACEMENT_3D('',#5607,#4651,#4652);
#3728=AXIS2_PLACEMENT_3D('',#5616,#4657,#4658);
#3729=AXIS2_PLACEMENT_3D('',#5622,#4662,#4663);
#3730=AXIS2_PLACEMENT_3D('',#5628,#4667,#4668);
#3731=AXIS2_PLACEMENT_3D('',#5634,#4672,#4673);
#3732=AXIS2_PLACEMENT_3D('',#5640,#4677,#4678);
#3733=AXIS2_PLACEMENT_3D('',#5643,#4681,#4682);
#3734=AXIS2_PLACEMENT_3D('',#5645,#4683,#4684);
#3735=AXIS2_PLACEMENT_3D('',#5646,#4685,#4686);
#3736=AXIS2_PLACEMENT_3D('',#5648,#4688,#4689);
#4561=DIRECTION('axis',(0.,0.,1.));
#4562=DIRECTION('refdir',(1.,0.,0.));
#4563=DIRECTION('center_axis',(0.,0.,1.));
#4564=DIRECTION('ref_axis',(1.,0.,0.));
#4565=DIRECTION('',(0.,0.,-1.));
#4566=DIRECTION('center_axis',(0.,0.,-1.));
#4567=DIRECTION('ref_axis',(1.,0.,0.));
#4568=DIRECTION('',(0.,0.,1.));
#4569=DIRECTION('center_axis',(0.,0.,1.));
#4570=DIRECTION('ref_axis',(1.,0.,0.));
#4571=DIRECTION('center_axis',(0.,0.,1.));
#4572=DIRECTION('ref_axis',(-1.,-1.22464679914735E-16,0.));
#4573=DIRECTION('',(0.,0.,1.));
#4574=DIRECTION('center_axis',(0.,0.,1.));
#4575=DIRECTION('ref_axis',(1.,0.,0.));
#4576=DIRECTION('',(0.,0.,-1.));
#4577=DIRECTION('center_axis',(0.,0.,-1.));
#4578=DIRECTION('ref_axis',(1.,0.,0.));
#4579=DIRECTION('center_axis',(0.,0.,1.));
#4580=DIRECTION('ref_axis',(1.,0.,0.));
#4581=DIRECTION('',(0.,0.,-1.));
#4582=DIRECTION('center_axis',(0.,0.,-1.));
#4583=DIRECTION('ref_axis',(1.,0.,0.));
#4584=DIRECTION('',(0.,0.,1.));
#4585=DIRECTION('center_axis',(0.,0.,1.));
#4586=DIRECTION('ref_axis',(1.,0.,0.));
#4587=DIRECTION('center_axis',(0.,0.,1.));
#4588=DIRECTION('ref_axis',(1.,0.,0.));
#4589=DIRECTION('',(0.,0.,-1.));
#4590=DIRECTION('center_axis',(0.,0.,-1.));
#4591=DIRECTION('ref_axis',(1.,0.,0.));
#4592=DIRECTION('',(0.,0.,1.));
#4593=DIRECTION('center_axis',(0.,0.,1.));
#4594=DIRECTION('ref_axis',(1.,0.,0.));
#4595=DIRECTION('center_axis',(0.,0.,1.));
#4596=DIRECTION('ref_axis',(1.,0.,0.));
#4597=DIRECTION('',(0.,0.,-1.));
#4598=DIRECTION('center_axis',(0.,0.,-1.));
#4599=DIRECTION('ref_axis',(1.,0.,0.));
#4600=DIRECTION('',(0.,0.,1.));
#4601=DIRECTION('center_axis',(0.,0.,1.));
#4602=DIRECTION('ref_axis',(1.,0.,0.));
#4603=DIRECTION('center_axis',(0.,0.,1.));
#4604=DIRECTION('ref_axis',(1.,0.,0.));
#4605=DIRECTION('',(0.,0.,-1.));
#4606=DIRECTION('center_axis',(0.,0.,-1.));
#4607=DIRECTION('ref_axis',(1.,0.,0.));
#4608=DIRECTION('',(0.,0.,1.));
#4609=DIRECTION('center_axis',(0.,0.,1.));
#4610=DIRECTION('ref_axis',(1.,0.,0.));
#4611=DIRECTION('center_axis',(0.,0.,1.));
#4612=DIRECTION('ref_axis',(1.,0.,0.));
#4613=DIRECTION('center_axis',(0.,0.,1.));
#4614=DIRECTION('ref_axis',(1.,0.,0.));
#4615=DIRECTION('center_axis',(0.,0.,1.));
#4616=DIRECTION('ref_axis',(1.,0.,0.));
#4617=DIRECTION('center_axis',(0.,0.,1.));
#4618=DIRECTION('ref_axis',(1.,0.,0.));
#4619=DIRECTION('center_axis',(0.,0.,1.));
#4620=DIRECTION('ref_axis',(1.,0.,0.));
#4621=DIRECTION('center_axis',(0.,0.,1.));
#4622=DIRECTION('ref_axis',(1.,0.,0.));
#4623=DIRECTION('center_axis',(0.,0.,1.));
#4624=DIRECTION('ref_axis',(1.,0.,0.));
#4625=DIRECTION('center_axis',(0.,0.,-1.));
#4626=DIRECTION('ref_axis',(1.,0.,0.));
#4627=DIRECTION('center_axis',(0.,0.,1.));
#4628=DIRECTION('ref_axis',(1.,0.,0.));
#4629=DIRECTION('center_axis',(0.,0.,1.));
#4630=DIRECTION('ref_axis',(1.,0.,0.));
#4631=DIRECTION('center_axis',(0.,0.,1.));
#4632=DIRECTION('ref_axis',(1.,0.,0.));
#4633=DIRECTION('center_axis',(0.,0.,1.));
#4634=DIRECTION('ref_axis',(1.,0.,0.));
#4635=DIRECTION('center_axis',(0.,0.,1.));
#4636=DIRECTION('ref_axis',(1.,0.,0.));
#4637=DIRECTION('center_axis',(0.,0.,1.));
#4638=DIRECTION('ref_axis',(1.,0.,0.));
#4639=DIRECTION('center_axis',(0.,0.,1.));
#4640=DIRECTION('ref_axis',(1.,0.,0.));
#4641=DIRECTION('center_axis',(0.,0.,1.));
#4642=DIRECTION('ref_axis',(1.,0.,0.));
#4643=DIRECTION('center_axis',(0.,0.,1.));
#4644=DIRECTION('ref_axis',(1.,0.,0.));
#4645=DIRECTION('center_axis',(0.,0.,1.));
#4646=DIRECTION('ref_axis',(1.,0.,0.));
#4647=DIRECTION('center_axis',(0.,0.,1.));
#4648=DIRECTION('ref_axis',(1.,0.,0.));
#4649=DIRECTION('center_axis',(0.,0.,1.));
#4650=DIRECTION('ref_axis',(1.,0.,0.));
#4651=DIRECTION('center_axis',(0.,1.,0.));
#4652=DIRECTION('ref_axis',(-1.,0.,0.));
#4653=DIRECTION('',(-1.,0.,0.));
#4654=DIRECTION('',(0.,0.,1.));
#4655=DIRECTION('',(-1.,0.,0.));
#4656=DIRECTION('',(0.,0.,1.));
#4657=DIRECTION('center_axis',(-0.866025403784438,0.500000000000001,0.));
#4658=DIRECTION('ref_axis',(-0.500000000000001,-0.866025403784438,0.));
#4659=DIRECTION('',(-0.500000000000001,-0.866025403784438,0.));
#4660=DIRECTION('',(-0.500000000000001,-0.866025403784438,0.));
#4661=DIRECTION('',(0.,0.,1.));
#4662=DIRECTION('center_axis',(-0.866025403784439,-0.5,0.));
#4663=DIRECTION('ref_axis',(0.5,-0.866025403784439,0.));
#4664=DIRECTION('',(0.5,-0.866025403784439,0.));
#4665=DIRECTION('',(0.5,-0.866025403784439,0.));
#4666=DIRECTION('',(0.,0.,1.));
#4667=DIRECTION('center_axis',(0.,-1.,0.));
#4668=DIRECTION('ref_axis',(1.,0.,0.));
#4669=DIRECTION('',(1.,0.,0.));
#4670=DIRECTION('',(1.,0.,0.));
#4671=DIRECTION('',(0.,0.,1.));
#4672=DIRECTION('center_axis',(0.866025403784439,0.5,0.));
#4673=DIRECTION('ref_axis',(-0.5,0.866025403784439,0.));
#4674=DIRECTION('',(-0.5,0.866025403784439,0.));
#4675=DIRECTION('',(0.,0.,1.));
#4676=DIRECTION('',(-0.5,0.866025403784439,0.));
#4677=DIRECTION('center_axis',(0.866025403784439,-0.5,0.));
#4678=DIRECTION('ref_axis',(0.5,0.866025403784439,0.));
#4679=DIRECTION('',(0.5,0.866025403784439,0.));
#4680=DIRECTION('',(0.5,0.866025403784439,0.));
#4681=DIRECTION('center_axis',(0.,0.,1.));
#4682=DIRECTION('ref_axis',(1.,0.,0.));
#4683=DIRECTION('center_axis',(0.,0.,-1.));
#4684=DIRECTION('ref_axis',(1.,0.,0.));
#4685=DIRECTION('center_axis',(0.,0.,1.));
#4686=DIRECTION('ref_axis',(1.,0.,0.));
#4687=DIRECTION('',(0.,0.,-1.));
#4688=DIRECTION('center_axis',(0.,0.,1.));
#4689=DIRECTION('ref_axis',(1.,0.,0.));
#5531=CARTESIAN_POINT('',(0.,0.,0.));
#5532=CARTESIAN_POINT('Origin',(6.5,-5.73205080756888,7.22132034));
#5533=CARTESIAN_POINT('',(6.89841665441537,-5.69649564641799,8.48132034));
#5534=CARTESIAN_POINT('',(6.89841665441537,-5.69649564641799,7.28132034));
#5535=CARTESIAN_POINT('',(6.89841665441537,-5.69649564641799,7.22132034));
#5536=CARTESIAN_POINT('',(6.33158334558463,-5.36923428297892,8.48132034));
#5537=CARTESIAN_POINT('Origin',(6.5,-5.73205080756888,8.48132034));
#5538=CARTESIAN_POINT('',(6.33158334558463,-5.36923428297892,7.28132034));
#5539=CARTESIAN_POINT('',(6.33158334558463,-5.36923428297892,7.22132034));
#5540=CARTESIAN_POINT('Origin',(6.5,-5.73205080756888,7.28132034));
#5541=CARTESIAN_POINT('Origin',(9.5,-4.,7.22132034));
#5542=CARTESIAN_POINT('',(9.27,-4.32726136343907,7.28132034));
#5543=CARTESIAN_POINT('',(9.27,-4.32726136343907,8.48132034));
#5544=CARTESIAN_POINT('',(9.27,-4.32726136343907,7.22132034));
#5545=CARTESIAN_POINT('',(9.27,-3.67273863656093,7.28132034));
#5546=CARTESIAN_POINT('Origin',(9.5,-4.,7.28132034));
#5547=CARTESIAN_POINT('',(9.27,-3.67273863656093,8.48132034));
#5548=CARTESIAN_POINT('',(9.27,-3.67273863656093,7.22132034));
#5549=CARTESIAN_POINT('Origin',(9.5,-4.,8.48132034));
#5550=CARTESIAN_POINT('Origin',(8.5,-2.26794919243112,7.22132034));
#5551=CARTESIAN_POINT('',(8.10158334558463,-2.30350435358201,8.48132034));
#5552=CARTESIAN_POINT('',(8.10158334558463,-2.30350435358201,7.28132034));
#5553=CARTESIAN_POINT('',(8.10158334558463,-2.30350435358201,7.22132034));
#5554=CARTESIAN_POINT('',(8.66841665441537,-2.63076571702108,8.48132034));
#5555=CARTESIAN_POINT('Origin',(8.5,-2.26794919243112,8.48132034));
#5556=CARTESIAN_POINT('',(8.66841665441537,-2.63076571702108,7.28132034));
#5557=CARTESIAN_POINT('',(8.66841665441537,-2.63076571702108,7.22132034));
#5558=CARTESIAN_POINT('Origin',(8.5,-2.26794919243112,7.28132034));
#5559=CARTESIAN_POINT('Origin',(6.5,-2.26794919243112,7.22132034));
#5560=CARTESIAN_POINT('',(6.33158334558463,-2.63076571702108,8.48132034));
#5561=CARTESIAN_POINT('',(6.33158334558463,-2.63076571702108,7.28132034));
#5562=CARTESIAN_POINT('',(6.33158334558463,-2.63076571702108,7.22132034));
#5563=CARTESIAN_POINT('',(6.89841665441537,-2.30350435358201,8.48132034));
#5564=CARTESIAN_POINT('Origin',(6.5,-2.26794919243112,8.48132034));
#5565=CARTESIAN_POINT('',(6.89841665441537,-2.30350435358201,7.28132034));
#5566=CARTESIAN_POINT('',(6.89841665441537,-2.30350435358201,7.22132034));
#5567=CARTESIAN_POINT('Origin',(6.5,-2.26794919243112,7.28132034));
#5568=CARTESIAN_POINT('Origin',(5.5,-4.,7.22132034));
#5569=CARTESIAN_POINT('',(5.73,-4.32726136343907,8.48132034));
#5570=CARTESIAN_POINT('',(5.73,-4.32726136343907,7.28132034));
#5571=CARTESIAN_POINT('',(5.73,-4.32726136343907,7.22132034));
#5572=CARTESIAN_POINT('',(5.73,-3.67273863656093,8.48132034));
#5573=CARTESIAN_POINT('Origin',(5.5,-4.,8.48132034));
#5574=CARTESIAN_POINT('',(5.73,-3.67273863656093,7.28132034));
#5575=CARTESIAN_POINT('',(5.73,-3.67273863656093,7.22132034));
#5576=CARTESIAN_POINT('Origin',(5.5,-4.,7.28132034));
#5577=CARTESIAN_POINT('Origin',(8.5,-5.73205080756888,7.22132034));
#5578=CARTESIAN_POINT('',(8.66841665441537,-5.36923428297892,8.48132034));
#5579=CARTESIAN_POINT('',(8.66841665441537,-5.36923428297892,7.28132034));
#5580=CARTESIAN_POINT('',(8.66841665441537,-5.36923428297892,7.22132034));
#5581=CARTESIAN_POINT('',(8.10158334558463,-5.69649564641799,8.48132034));
#5582=CARTESIAN_POINT('Origin',(8.5,-5.73205080756888,8.48132034));
#5583=CARTESIAN_POINT('',(8.10158334558463,-5.69649564641799,7.28132034));
#5584=CARTESIAN_POINT('',(8.10158334558463,-5.69649564641799,7.22132034));
#5585=CARTESIAN_POINT('Origin',(8.5,-5.73205080756888,7.28132034));
#5586=CARTESIAN_POINT('Origin',(7.5,-4.,8.48132034));
#5587=CARTESIAN_POINT('Origin',(7.5,-4.,8.48132034));
#5588=CARTESIAN_POINT('Origin',(7.5,-4.,8.48132034));
#5589=CARTESIAN_POINT('Origin',(7.5,-4.,8.48132034));
#5590=CARTESIAN_POINT('Origin',(7.5,-4.,8.48132034));
#5591=CARTESIAN_POINT('Origin',(7.5,-4.,8.48132034));
#5592=CARTESIAN_POINT('Origin',(7.5,-4.,8.48132034));
#5593=CARTESIAN_POINT('',(7.075,-4.,8.48132034));
#5594=CARTESIAN_POINT('Origin',(7.5,-4.,8.48132034));
#5595=CARTESIAN_POINT('Origin',(7.5,-4.,7.28132034));
#5596=CARTESIAN_POINT('Origin',(7.5,-4.,7.28132034));
#5597=CARTESIAN_POINT('Origin',(7.5,-4.,7.28132034));
#5598=CARTESIAN_POINT('Origin',(7.5,-4.,7.28132034));
#5599=CARTESIAN_POINT('Origin',(7.5,-4.,7.28132034));
#5600=CARTESIAN_POINT('Origin',(7.5,-4.,7.28132034));
#5601=CARTESIAN_POINT('Origin',(7.5,-4.,7.28132034));
#5602=CARTESIAN_POINT('Origin',(7.5,-4.,7.28132034));
#5603=CARTESIAN_POINT('Origin',(7.5,-4.,7.28132034));
#5604=CARTESIAN_POINT('Origin',(7.5,-4.,7.28132034));
#5605=CARTESIAN_POINT('Origin',(7.5,-4.,7.28132034));
#5606=CARTESIAN_POINT('Origin',(7.5,-4.,7.28132034));
#5607=CARTESIAN_POINT('Origin',(7.87527767497326,-3.35,7.27132034));
#5608=CARTESIAN_POINT('',(7.87527767497326,-3.35,7.28132034));
#5609=CARTESIAN_POINT('',(7.12472232502674,-3.35,7.28132034));
#5610=CARTESIAN_POINT('',(7.68763883748663,-3.35,7.28132034));
#5611=CARTESIAN_POINT('',(7.87527767497326,-3.35,7.97132034));
#5612=CARTESIAN_POINT('',(7.87527767497326,-3.35,7.27132034));
#5613=CARTESIAN_POINT('',(7.12472232502674,-3.35,7.97132034));
#5614=CARTESIAN_POINT('',(7.87527767497326,-3.35,7.97132034));
#5615=CARTESIAN_POINT('',(7.12472232502674,-3.35,7.27132034));
#5616=CARTESIAN_POINT('Origin',(7.12472232502674,-3.35,7.27132034));
#5617=CARTESIAN_POINT('',(6.74944465005349,-4.,7.28132034));
#5618=CARTESIAN_POINT('',(7.03090290628343,-3.5125,7.28132034));
#5619=CARTESIAN_POINT('',(6.74944465005349,-4.,7.97132034));
#5620=CARTESIAN_POINT('',(7.12472232502674,-3.35,7.97132034));
#5621=CARTESIAN_POINT('',(6.74944465005349,-4.,7.27132034));
#5622=CARTESIAN_POINT('Origin',(6.74944465005349,-4.,7.27132034));
#5623=CARTESIAN_POINT('',(7.12472232502674,-4.65,7.28132034));
#5624=CARTESIAN_POINT('',(6.8432640687968,-4.1625,7.28132034));
#5625=CARTESIAN_POINT('',(7.12472232502674,-4.65,7.97132034));
#5626=CARTESIAN_POINT('',(6.74944465005349,-4.,7.97132034));
#5627=CARTESIAN_POINT('',(7.12472232502674,-4.65,7.27132034));
#5628=CARTESIAN_POINT('Origin',(7.12472232502674,-4.65,7.27132034));
#5629=CARTESIAN_POINT('',(7.87527767497326,-4.65,7.28132034));
#5630=CARTESIAN_POINT('',(7.31236116251337,-4.65,7.28132034));
#5631=CARTESIAN_POINT('',(7.87527767497326,-4.65,7.97132034));
#5632=CARTESIAN_POINT('',(7.12472232502674,-4.65,7.97132034));
#5633=CARTESIAN_POINT('',(7.87527767497326,-4.65,7.27132034));
#5634=CARTESIAN_POINT('Origin',(8.25055534994651,-4.,7.27132034));
#5635=CARTESIAN_POINT('',(8.25055534994651,-4.,7.28132034));
#5636=CARTESIAN_POINT('',(8.1567359312032,-3.8375,7.28132034));
#5637=CARTESIAN_POINT('',(8.25055534994651,-4.,7.97132034));
#5638=CARTESIAN_POINT('',(8.25055534994651,-4.,7.27132034));
#5639=CARTESIAN_POINT('',(8.25055534994651,-4.,7.97132034));
#5640=CARTESIAN_POINT('Origin',(7.87527767497326,-4.65,7.27132034));
#5641=CARTESIAN_POINT('',(7.96909709371657,-4.4875,7.28132034));
#5642=CARTESIAN_POINT('',(7.87527767497326,-4.65,7.97132034));
#5643=CARTESIAN_POINT('Origin',(7.5,-4.,7.97132034));
#5644=CARTESIAN_POINT('',(7.075,-4.,7.97132034));
#5645=CARTESIAN_POINT('Origin',(7.5,-4.,7.97132034));
#5646=CARTESIAN_POINT('Origin',(7.5,-4.,7.28132034));
#5647=CARTESIAN_POINT('',(7.075,-4.,7.28132034));
#5648=CARTESIAN_POINT('Origin',(7.5,-4.,7.28132034));
#5687=UNCERTAINTY_MEASURE_WITH_UNIT(LENGTH_MEASURE(0.001),#5703,
'DISTANCE_ACCURACY_VALUE',
'Maximum model space distance between geometric entities at asserted c
onnectivities');
#5688=UNCERTAINTY_MEASURE_WITH_UNIT(LENGTH_MEASURE(0.001),#5703,
'DISTANCE_ACCURACY_VALUE',
'Maximum model space distance between geometric entities at asserted c
onnectivities');
#5701=(
GEOMETRIC_REPRESENTATION_CONTEXT(3)
GLOBAL_UNCERTAINTY_ASSIGNED_CONTEXT((#5687))
GLOBAL_UNIT_ASSIGNED_CONTEXT((#5703,#5705,#5706))
REPRESENTATION_CONTEXT('','3D')
);
#5702=(
GEOMETRIC_REPRESENTATION_CONTEXT(3)
GLOBAL_UNCERTAINTY_ASSIGNED_CONTEXT((#5688))
GLOBAL_UNIT_ASSIGNED_CONTEXT((#5703,#5705,#5706))
REPRESENTATION_CONTEXT('','3D')
);
#5703=(
LENGTH_UNIT()
NAMED_UNIT(*)
SI_UNIT(.CENTI.,.METRE.)
);
#5705=(
NAMED_UNIT(*)
PLANE_ANGLE_UNIT()
SI_UNIT($,.RADIAN.)
);
#5706=(
NAMED_UNIT(*)
SI_UNIT($,.STERADIAN.)
SOLID_ANGLE_UNIT()
);
#5719=SHAPE_DEFINITION_REPRESENTATION(#5732,#5771);
#5732=PRODUCT_DEFINITION_SHAPE('',$,#5785);
#5771=SHAPE_REPRESENTATION('',(#3688),#5701);
#5772=PRODUCT_DEFINITION_CONTEXT('part definition',#5813,'design');
#5785=PRODUCT_DEFINITION('Captive-nut hand knob',
'Captive-nut hand knob',#5798,#5772);
#5798=PRODUCT_DEFINITION_FORMATION('',$,#5827);
#5813=APPLICATION_CONTEXT(
'Core Data for Automotive Mechanical Design Process');
#5814=PRODUCT_CONTEXT('part definition',#5813,'mechanical');
#5827=PRODUCT('Captive-nut hand knob','Captive-nut hand knob',
'Captive-nut hand knob',(#5814));
#5898=COLOUR_RGB('Black',0.12,0.14,0.17);
#5899=FILL_AREA_STYLE_COLOUR('',#5898);
#5900=FILL_AREA_STYLE('',(#5899));
#5901=SURFACE_STYLE_FILL_AREA(#5900);
#5902=SURFACE_SIDE_STYLE('',(#5901));
#5903=SURFACE_STYLE_USAGE(.BOTH.,#5902);
#5904=PRESENTATION_STYLE_ASSIGNMENT((#5903));
ENDSEC;
END-ISO-10303-21;
